ISO-10303-21;
HEADER;
/* Generated by software containing ST-Developer
 * from STEP Tools, Inc. (www.steptools.com) 
 */

FILE_DESCRIPTION(
/* description */ ('PAT-091'),
/* implementation_level */ '2;1');

FILE_NAME(
/* name */ 'Plain pivot bush (5).step',
/* time_stamp */ '2026-10-27T15:34:44-07:00',
/* author */ (''),
/* organization */ (''),
/* preprocessor_version */ 'ST-DEVELOPER v20.2',
/* originating_system */ 'Autodesk Translation Framework v15.17.0.0',
/* authorisation */ '');

FILE_SCHEMA (('AUTOMOTIVE_DESIGN { 1 0 10303 214 3 1 1 }'));
ENDSEC;

DATA;
#10=MECHANICAL_DESIGN_GEOMETRIC_PRESENTATION_REPRESENTATION('',(#1034),#25100);
#814=SHAPE_REPRESENTATION_RELATIONSHIP('SRR','None',#25580,#924);
#924=ADVANCED_BREP_SHAPE_REPRESENTATION('',(#1156),#25050);
#1034=STYLED_ITEM('',(#26177),#1156);
#1156=MANIFOLD_SOLID_BREP('Body1',#13313);
#1506=FACE_BOUND('',#3669,.T.);
#1507=FACE_BOUND('',#3671,.T.);
#1917=PLANE('',#15594);
#1918=PLANE('',#15595);
#2557=FACE_OUTER_BOUND('',#3666,.T.);
#2558=FACE_OUTER_BOUND('',#3667,.T.);
#2559=FACE_OUTER_BOUND('',#3668,.T.);
#2560=FACE_OUTER_BOUND('',#3670,.T.);
#3666=EDGE_LOOP('',(#10966,#10967,#10968,#10969));
#3667=EDGE_LOOP('',(#10970,#10971,#10972,#10973));
#3668=EDGE_LOOP('',(#10974));
#3669=EDGE_LOOP('',(#10975));
#3670=EDGE_LOOP('',(#10976));
#3671=EDGE_LOOP('',(#10977));
#4681=LINE('',#23256,#5421);
#4682=LINE('',#23262,#5422);
#5421=VECTOR('',#19035,0.605);
#5422=VECTOR('',#19042,1.);
#6040=CIRCLE('',#15589,0.605);
#6041=CIRCLE('',#15590,0.605);
#6042=CIRCLE('',#15592,1.);
#6043=CIRCLE('',#15593,1.);
#7045=VERTEX_POINT('',#23253);
#7046=VERTEX_POINT('',#23255);
#7047=VERTEX_POINT('',#23259);
#7048=VERTEX_POINT('',#23261);
#8418=EDGE_CURVE('',#7045,#7045,#6040,.T.);
#8419=EDGE_CURVE('',#7045,#7046,#4681,.T.);
#8420=EDGE_CURVE('',#7046,#7046,#6041,.T.);
#8421=EDGE_CURVE('',#7047,#7047,#6042,.T.);
#8422=EDGE_CURVE('',#7047,#7048,#4682,.T.);
#8423=EDGE_CURVE('',#7048,#7048,#6043,.T.);
#10966=ORIENTED_EDGE('',*,*,#8418,.F.);
#10967=ORIENTED_EDGE('',*,*,#8419,.T.);
#10968=ORIENTED_EDGE('',*,*,#8420,.T.);
#10969=ORIENTED_EDGE('',*,*,#8419,.F.);
#10970=ORIENTED_EDGE('',*,*,#8421,.F.);
#10971=ORIENTED_EDGE('',*,*,#8422,.T.);
#10972=ORIENTED_EDGE('',*,*,#8423,.T.);
#10973=ORIENTED_EDGE('',*,*,#8422,.F.);
#10974=ORIENTED_EDGE('',*,*,#8421,.T.);
#10975=ORIENTED_EDGE('',*,*,#8418,.T.);
#10976=ORIENTED_EDGE('',*,*,#8423,.F.);
#10977=ORIENTED_EDGE('',*,*,#8420,.F.);
#12283=CYLINDRICAL_SURFACE('',#15588,0.605);
#12284=CYLINDRICAL_SURFACE('',#15591,1.);
#12924=ADVANCED_FACE('',(#2557),#12283,.F.);
#12925=ADVANCED_FACE('',(#2558),#12284,.T.);
#12926=ADVANCED_FACE('',(#2559,#1506),#1917,.T.);
#12927=ADVANCED_FACE('',(#2560,#1507),#1918,.F.);
#13313=CLOSED_SHELL('',(#12924,#12925,#12926,#12927));
#15587=AXIS2_PLACEMENT_3D('',#23251,#19029,#19030);
#15588=AXIS2_PLACEMENT_3D('',#23252,#19031,#19032);
#15589=AXIS2_PLACEMENT_3D('',#23254,#19033,#19034);
#15590=AXIS2_PLACEMENT_3D('',#23257,#19036,#19037);
#15591=AXIS2_PLACEMENT_3D('',#23258,#19038,#19039);
#15592=AXIS2_PLACEMENT_3D('',#23260,#19040,#19041);
#15593=AXIS2_PLACEMENT_3D('',#23263,#19043,#19044);
#15594=AXIS2_PLACEMENT_3D('',#23264,#19045,#19046);
#15595=AXIS2_PLACEMENT_3D('',#23265,#19047,#19048);
#19029=DIRECTION('axis',(0.,0.,1.));
#19030=DIRECTION('refdir',(1.,0.,0.));
#19031=DIRECTION('center_axis',(0.,1.,0.));
#19032=DIRECTION('ref_axis',(1.,0.,0.));
#19033=DIRECTION('center_axis',(0.,-1.,0.));
#19034=DIRECTION('ref_axis',(1.,0.,0.));
#19035=DIRECTION('',(0.,-1.,0.));
#19036=DIRECTION('center_axis',(0.,-1.,0.));
#19037=DIRECTION('ref_axis',(1.,0.,0.));
#19038=DIRECTION('center_axis',(0.,1.,0.));
#19039=DIRECTION('ref_axis',(1.,0.,0.));
#19040=DIRECTION('center_axis',(0.,1.,0.));
#19041=DIRECTION('ref_axis',(1.,0.,0.));
#19042=DIRECTION('',(0.,-1.,0.));
#19043=DIRECTION('center_axis',(0.,1.,0.));
#19044=DIRECTION('ref_axis',(1.,0.,0.));
#19045=DIRECTION('center_axis',(0.,1.,0.));
#19046=DIRECTION('ref_axis',(1.,0.,0.));
#19047=DIRECTION('center_axis',(0.,1.,0.));
#19048=DIRECTION('ref_axis',(1.,0.,0.));
#23251=CARTESIAN_POINT('',(0.,0.,0.));
#23252=CARTESIAN_POINT('Origin',(19.3649167310371,5.,8.));
#23253=CARTESIAN_POINT('',(18.7599167310371,6.,8.));
#23254=CARTESIAN_POINT('Origin',(19.3649167310371,6.,8.));
#23255=CARTESIAN_POINT('',(18.7599167310371,5.,8.));
#23256=CARTESIAN_POINT('',(18.7599167310371,5.,8.));
#23257=CARTESIAN_POINT('Origin',(19.3649167310371,5.,8.));
#23258=CARTESIAN_POINT('Origin',(19.3649167310371,5.,8.));
#23259=CARTESIAN_POINT('',(18.3649167310371,6.,8.));
#23260=CARTESIAN_POINT('Origin',(19.3649167310371,6.,8.));
#23261=CARTESIAN_POINT('',(18.3649167310371,5.,8.));
#23262=CARTESIAN_POINT('',(18.3649167310371,5.,8.));
#23263=CARTESIAN_POINT('Origin',(19.3649167310371,5.,8.));
#23264=CARTESIAN_POINT('Origin',(19.3649167310371,6.,8.));
#23265=CARTESIAN_POINT('Origin',(19.3649167310371,5.,8.));
#24929=UNCERTAINTY_MEASURE_WITH_UNIT(LENGTH_MEASURE(0.001),#25101,
'DISTANCE_ACCURACY_VALUE',
'Maximum model space distance between geometric entities at asserted c
onnectivities');
#24979=UNCERTAINTY_MEASURE_WITH_UNIT(LENGTH_MEASURE(0.001),#25101,
'DISTANCE_ACCURACY_VALUE',
'Maximum model space distance between geometric entities at asserted c
onnectivities');
#25050=(
GEOMETRIC_REPRESENTATION_CONTEXT(3)
GLOBAL_UNCERTAINTY_ASSIGNED_CONTEXT((#24929))
GLOBAL_UNIT_ASSIGNED_CONTEXT((#25101,#25103,#25104))
REPRESENTATION_CONTEXT('','3D')
);
#25100=(
GEOMETRIC_REPRESENTATION_CONTEXT(3)
GLOBAL_UNCERTAINTY_ASSIGNED_CONTEXT((#24979))
GLOBAL_UNIT_ASSIGNED_CONTEXT((#25101,#25103,#25104))
REPRESENTATION_CONTEXT('','3D')
);
#25101=(
LENGTH_UNIT()
NAMED_UNIT(*)
SI_UNIT(.CENTI.,.METRE.)
);
#25103=(
NAMED_UNIT(*)
PLANE_ANGLE_UNIT()
SI_UNIT($,.RADIAN.)
);
#25104=(
NAMED_UNIT(*)
SI_UNIT($,.STERADIAN.)
SOLID_ANGLE_UNIT()
);
#25175=SHAPE_DEFINITION_REPRESENTATION(#25297,#25580);
#25297=PRODUCT_DEFINITION_SHAPE('',$,#25701);
#25580=SHAPE_REPRESENTATION('',(#15587),#25050);
#25630=PRODUCT_DEFINITION_CONTEXT('part definition',#25992,'design');
#25701=PRODUCT_DEFINITION('Plain pivot bush (5)','Plain pivot bush (5)',#25821,
#25630);
#25821=PRODUCT_DEFINITION_FORMATION('',$,#26064);
#25992=APPLICATION_CONTEXT(
'Core Data for Automotive Mechanical Design Process');
#25993=PRODUCT_CONTEXT('part definition',#25992,'mechanical');
#26064=PRODUCT('Plain pivot bush (5)','Plain pivot bush (5)',
'Plain pivot bush (5)',(#25993));
#26171=COLOUR_RGB('Light Blue',0.38,0.62,0.78);
#26172=FILL_AREA_STYLE_COLOUR('',#26171);
#26173=FILL_AREA_STYLE('',(#26172));
#26174=SURFACE_STYLE_FILL_AREA(#26173);
#26175=SURFACE_SIDE_STYLE('',(#26174));
#26176=SURFACE_STYLE_USAGE(.BOTH.,#26175);
#26177=PRESENTATION_STYLE_ASSIGNMENT((#26176));
ENDSEC;
END-ISO-10303-21;
